ISO-10303-21;
HEADER;
/* Generated by software containing ST-Developer
 * from STEP Tools, Inc. (www.steptools.com) 
 */

FILE_DESCRIPTION(
/* description */ ('Located fixture plate with toggle clamp'),
/* implementation_level */ '2;1');

FILE_NAME(
/* name */ 'Hex Nut - M6.step',
/* time_stamp */ '2026-10-27T21:36:12-07:00',
/* author */ (''),
/* organization */ (''),
/* preprocessor_version */ 'ST-DEVELOPER v20.2',
/* originating_system */ 'Autodesk Translation Framework v15.17.0.0',
/* authorisation */ '');

FILE_SCHEMA (('AUTOMOTIVE_DESIGN { 1 0 10303 214 3 1 1 }'));
ENDSEC;

DATA;
#10=MECHANICAL_DESIGN_GEOMETRIC_PRESENTATION_REPRESENTATION('',(#328),#9285);
#210=(
BOUNDED_CURVE()
B_SPLINE_CURVE(2,(#8265,#8266,#8267),.UNSPECIFIED.,.F.,.F.)
B_SPLINE_CURVE_WITH_KNOTS((3,3),(0.144988513094728,0.791574906712449),
 .UNSPECIFIED.)
CURVE()
GEOMETRIC_REPRESENTATION_ITEM()
RATIONAL_B_SPLINE_CURVE((1.09282032302755,1.26188021535082,1.09282032302931))
REPRESENTATION_ITEM('')
);
#211=(
BOUNDED_CURVE()
B_SPLINE_CURVE(2,(#8269,#8270,#8271),.UNSPECIFIED.,.F.,.F.)
B_SPLINE_CURVE_WITH_KNOTS((3,3),(0.144988513094728,0.791574906712449),
 .UNSPECIFIED.)
CURVE()
GEOMETRIC_REPRESENTATION_ITEM()
RATIONAL_B_SPLINE_CURVE((1.09282032302755,1.26188021535082,1.09282032302931))
REPRESENTATION_ITEM('')
);
#212=(
BOUNDED_CURVE()
B_SPLINE_CURVE(2,(#8276,#8277,#8278),.UNSPECIFIED.,.F.,.F.)
B_SPLINE_CURVE_WITH_KNOTS((3,3),(0.144988513094728,0.791574906712449),
 .UNSPECIFIED.)
CURVE()
GEOMETRIC_REPRESENTATION_ITEM()
RATIONAL_B_SPLINE_CURVE((1.09282032302755,1.26188021535082,1.09282032302931))
REPRESENTATION_ITEM('')
);
#213=(
BOUNDED_CURVE()
B_SPLINE_CURVE(2,(#8280,#8281,#8282),.UNSPECIFIED.,.F.,.F.)
B_SPLINE_CURVE_WITH_KNOTS((3,3),(0.144988513094728,0.791574906712449),
 .UNSPECIFIED.)
CURVE()
GEOMETRIC_REPRESENTATION_ITEM()
RATIONAL_B_SPLINE_CURVE((1.09282032302755,1.26188021535082,1.09282032302931))
REPRESENTATION_ITEM('')
);
#214=(
BOUNDED_CURVE()
B_SPLINE_CURVE(2,(#8284,#8285,#8286),.UNSPECIFIED.,.F.,.F.)
B_SPLINE_CURVE_WITH_KNOTS((3,3),(0.144988513094728,0.791574906712449),
 .UNSPECIFIED.)
CURVE()
GEOMETRIC_REPRESENTATION_ITEM()
RATIONAL_B_SPLINE_CURVE((1.09282032302755,1.26188021535082,1.09282032302931))
REPRESENTATION_ITEM('')
);
#215=(
BOUNDED_CURVE()
B_SPLINE_CURVE(2,(#8287,#8288,#8289),.UNSPECIFIED.,.F.,.F.)
B_SPLINE_CURVE_WITH_KNOTS((3,3),(0.144988513094728,0.791574906712449),
 .UNSPECIFIED.)
CURVE()
GEOMETRIC_REPRESENTATION_ITEM()
RATIONAL_B_SPLINE_CURVE((1.09282032302755,1.26188021535082,1.09282032302931))
REPRESENTATION_ITEM('')
);
#216=(
BOUNDED_CURVE()
B_SPLINE_CURVE(2,(#8296,#8297,#8298),.UNSPECIFIED.,.F.,.F.)
B_SPLINE_CURVE_WITH_KNOTS((3,3),(0.144988513094728,0.791574906712449),
 .UNSPECIFIED.)
CURVE()
GEOMETRIC_REPRESENTATION_ITEM()
RATIONAL_B_SPLINE_CURVE((1.09282032302755,1.26188021535082,1.09282032302931))
REPRESENTATION_ITEM('')
);
#217=(
BOUNDED_CURVE()
B_SPLINE_CURVE(2,(#8300,#8301,#8302),.UNSPECIFIED.,.F.,.F.)
B_SPLINE_CURVE_WITH_KNOTS((3,3),(0.144988513094727,0.791574906712449),
 .UNSPECIFIED.)
CURVE()
GEOMETRIC_REPRESENTATION_ITEM()
RATIONAL_B_SPLINE_CURVE((1.09282032302755,1.26188021535082,1.09282032302931))
REPRESENTATION_ITEM('')
);
#218=(
BOUNDED_CURVE()
B_SPLINE_CURVE(2,(#8304,#8305,#8306),.UNSPECIFIED.,.F.,.F.)
B_SPLINE_CURVE_WITH_KNOTS((3,3),(0.144988513094728,0.791574906712449),
 .UNSPECIFIED.)
CURVE()
GEOMETRIC_REPRESENTATION_ITEM()
RATIONAL_B_SPLINE_CURVE((1.09282032302755,1.26188021535082,1.09282032302931))
REPRESENTATION_ITEM('')
);
#219=(
BOUNDED_CURVE()
B_SPLINE_CURVE(2,(#8308,#8309,#8310),.UNSPECIFIED.,.F.,.F.)
B_SPLINE_CURVE_WITH_KNOTS((3,3),(0.144988513094728,0.791574906712449),
 .UNSPECIFIED.)
CURVE()
GEOMETRIC_REPRESENTATION_ITEM()
RATIONAL_B_SPLINE_CURVE((1.09282032302755,1.26188021535082,1.09282032302931))
REPRESENTATION_ITEM('')
);
#220=(
BOUNDED_CURVE()
B_SPLINE_CURVE(2,(#8312,#8313,#8314),.UNSPECIFIED.,.F.,.F.)
B_SPLINE_CURVE_WITH_KNOTS((3,3),(0.144988513094728,0.791574906712449),
 .UNSPECIFIED.)
CURVE()
GEOMETRIC_REPRESENTATION_ITEM()
RATIONAL_B_SPLINE_CURVE((1.09282032302755,1.26188021535082,1.09282032302931))
REPRESENTATION_ITEM('')
);
#221=(
BOUNDED_CURVE()
B_SPLINE_CURVE(2,(#8315,#8316,#8317),.UNSPECIFIED.,.F.,.F.)
B_SPLINE_CURVE_WITH_KNOTS((3,3),(0.144988513094727,0.791574906712449),
 .UNSPECIFIED.)
CURVE()
GEOMETRIC_REPRESENTATION_ITEM()
RATIONAL_B_SPLINE_CURVE((1.09282032302755,1.26188021535082,1.09282032302931))
REPRESENTATION_ITEM('')
);
#256=CONICAL_SURFACE('',#5703,0.576175134594813,1.0471975511966);
#257=CONICAL_SURFACE('',#5705,0.576175134594813,1.0471975511966);
#280=SHAPE_REPRESENTATION_RELATIONSHIP('SRR','None',#9403,#304);
#304=ADVANCED_BREP_SHAPE_REPRESENTATION('',(#351),#9265);
#328=STYLED_ITEM('',(#9619),#351);
#351=MANIFOLD_SOLID_BREP('Body1',#5177);
#449=FACE_BOUND('',#1193,.T.);
#450=FACE_BOUND('',#1195,.T.);
#566=PLANE('',#5707);
#567=PLANE('',#5708);
#568=PLANE('',#5709);
#569=PLANE('',#5713);
#570=PLANE('',#5714);
#571=PLANE('',#5715);
#572=PLANE('',#5716);
#573=PLANE('',#5717);
#805=FACE_OUTER_BOUND('',#1183,.T.);
#806=FACE_OUTER_BOUND('',#1184,.T.);
#807=FACE_OUTER_BOUND('',#1185,.T.);
#808=FACE_OUTER_BOUND('',#1186,.T.);
#809=FACE_OUTER_BOUND('',#1187,.T.);
#810=FACE_OUTER_BOUND('',#1188,.T.);
#811=FACE_OUTER_BOUND('',#1189,.T.);
#812=FACE_OUTER_BOUND('',#1190,.T.);
#813=FACE_OUTER_BOUND('',#1191,.T.);
#814=FACE_OUTER_BOUND('',#1192,.T.);
#815=FACE_OUTER_BOUND('',#1194,.T.);
#1183=EDGE_LOOP('',(#4126,#4127,#4128,#4129,#4130,#4131,#4132,#4133,#4134));
#1184=EDGE_LOOP('',(#4135,#4136,#4137,#4138,#4139,#4140,#4141,#4142,#4143));
#1185=EDGE_LOOP('',(#4144,#4145,#4146,#4147));
#1186=EDGE_LOOP('',(#4148,#4149,#4150,#4151));
#1187=EDGE_LOOP('',(#4152,#4153,#4154,#4155));
#1188=EDGE_LOOP('',(#4156,#4157,#4158,#4159));
#1189=EDGE_LOOP('',(#4160,#4161,#4162,#4163));
#1190=EDGE_LOOP('',(#4164,#4165,#4166,#4167));
#1191=EDGE_LOOP('',(#4168,#4169,#4170,#4171));
#1192=EDGE_LOOP('',(#4172));
#1193=EDGE_LOOP('',(#4173));
#1194=EDGE_LOOP('',(#4174));
#1195=EDGE_LOOP('',(#4175));
#1483=CIRCLE('',#5704,0.475);
#1484=CIRCLE('',#5706,0.475);
#1485=CIRCLE('',#5711,0.25175);
#1486=CIRCLE('',#5712,0.25175);
#1796=LINE('',#8273,#2206);
#1797=LINE('',#8294,#2207);
#1798=LINE('',#8319,#2208);
#1799=LINE('',#8320,#2209);
#1800=LINE('',#8322,#2210);
#1801=LINE('',#8324,#2211);
#1802=LINE('',#8329,#2212);
#1803=LINE('',#8332,#2213);
#1804=LINE('',#8334,#2214);
#2206=VECTOR('',#6730,0.576175134594813);
#2207=VECTOR('',#6737,0.576175134594813);
#2208=VECTOR('',#6740,1.);
#2209=VECTOR('',#6741,1.);
#2210=VECTOR('',#6744,1.);
#2211=VECTOR('',#6747,1.);
#2212=VECTOR('',#6752,0.3);
#2213=VECTOR('',#6757,1.);
#2214=VECTOR('',#6760,1.);
#2613=VERTEX_POINT('',#8263);
#2614=VERTEX_POINT('',#8264);
#2615=VERTEX_POINT('',#8268);
#2616=VERTEX_POINT('',#8272);
#2617=VERTEX_POINT('',#8275);
#2618=VERTEX_POINT('',#8279);
#2619=VERTEX_POINT('',#8283);
#2620=VERTEX_POINT('',#8291);
#2621=VERTEX_POINT('',#8293);
#2622=VERTEX_POINT('',#8295);
#2623=VERTEX_POINT('',#8299);
#2624=VERTEX_POINT('',#8303);
#2625=VERTEX_POINT('',#8307);
#2626=VERTEX_POINT('',#8311);
#2627=VERTEX_POINT('',#8326);
#2628=VERTEX_POINT('',#8328);
#3151=EDGE_CURVE('',#2613,#2614,#210,.T.);
#3152=EDGE_CURVE('',#2615,#2613,#211,.T.);
#3153=EDGE_CURVE('',#2615,#2616,#1796,.T.);
#3154=EDGE_CURVE('',#2616,#2616,#1483,.T.);
#3155=EDGE_CURVE('',#2617,#2615,#212,.T.);
#3156=EDGE_CURVE('',#2618,#2617,#213,.T.);
#3157=EDGE_CURVE('',#2619,#2618,#214,.T.);
#3158=EDGE_CURVE('',#2614,#2619,#215,.T.);
#3159=EDGE_CURVE('',#2620,#2620,#1484,.T.);
#3160=EDGE_CURVE('',#2620,#2621,#1797,.T.);
#3161=EDGE_CURVE('',#2622,#2621,#216,.T.);
#3162=EDGE_CURVE('',#2623,#2622,#217,.T.);
#3163=EDGE_CURVE('',#2624,#2623,#218,.T.);
#3164=EDGE_CURVE('',#2625,#2624,#219,.T.);
#3165=EDGE_CURVE('',#2626,#2625,#220,.T.);
#3166=EDGE_CURVE('',#2621,#2626,#221,.T.);
#3167=EDGE_CURVE('',#2617,#2626,#1798,.T.);
#3168=EDGE_CURVE('',#2618,#2625,#1799,.T.);
#3169=EDGE_CURVE('',#2615,#2621,#1800,.T.);
#3170=EDGE_CURVE('',#2613,#2622,#1801,.T.);
#3171=EDGE_CURVE('',#2627,#2627,#1485,.F.);
#3172=EDGE_CURVE('',#2627,#2628,#1802,.T.);
#3173=EDGE_CURVE('',#2628,#2628,#1486,.F.);
#3174=EDGE_CURVE('',#2614,#2623,#1803,.T.);
#3175=EDGE_CURVE('',#2619,#2624,#1804,.T.);
#4126=ORIENTED_EDGE('',*,*,#3151,.F.);
#4127=ORIENTED_EDGE('',*,*,#3152,.F.);
#4128=ORIENTED_EDGE('',*,*,#3153,.T.);
#4129=ORIENTED_EDGE('',*,*,#3154,.F.);
#4130=ORIENTED_EDGE('',*,*,#3153,.F.);
#4131=ORIENTED_EDGE('',*,*,#3155,.F.);
#4132=ORIENTED_EDGE('',*,*,#3156,.F.);
#4133=ORIENTED_EDGE('',*,*,#3157,.F.);
#4134=ORIENTED_EDGE('',*,*,#3158,.F.);
#4135=ORIENTED_EDGE('',*,*,#3159,.F.);
#4136=ORIENTED_EDGE('',*,*,#3160,.T.);
#4137=ORIENTED_EDGE('',*,*,#3161,.F.);
#4138=ORIENTED_EDGE('',*,*,#3162,.F.);
#4139=ORIENTED_EDGE('',*,*,#3163,.F.);
#4140=ORIENTED_EDGE('',*,*,#3164,.F.);
#4141=ORIENTED_EDGE('',*,*,#3165,.F.);
#4142=ORIENTED_EDGE('',*,*,#3166,.F.);
#4143=ORIENTED_EDGE('',*,*,#3160,.F.);
#4144=ORIENTED_EDGE('',*,*,#3156,.T.);
#4145=ORIENTED_EDGE('',*,*,#3167,.T.);
#4146=ORIENTED_EDGE('',*,*,#3165,.T.);
#4147=ORIENTED_EDGE('',*,*,#3168,.F.);
#4148=ORIENTED_EDGE('',*,*,#3155,.T.);
#4149=ORIENTED_EDGE('',*,*,#3169,.T.);
#4150=ORIENTED_EDGE('',*,*,#3166,.T.);
#4151=ORIENTED_EDGE('',*,*,#3167,.F.);
#4152=ORIENTED_EDGE('',*,*,#3152,.T.);
#4153=ORIENTED_EDGE('',*,*,#3170,.T.);
#4154=ORIENTED_EDGE('',*,*,#3161,.T.);
#4155=ORIENTED_EDGE('',*,*,#3169,.F.);
#4156=ORIENTED_EDGE('',*,*,#3171,.F.);
#4157=ORIENTED_EDGE('',*,*,#3172,.T.);
#4158=ORIENTED_EDGE('',*,*,#3173,.T.);
#4159=ORIENTED_EDGE('',*,*,#3172,.F.);
#4160=ORIENTED_EDGE('',*,*,#3151,.T.);
#4161=ORIENTED_EDGE('',*,*,#3174,.T.);
#4162=ORIENTED_EDGE('',*,*,#3162,.T.);
#4163=ORIENTED_EDGE('',*,*,#3170,.F.);
#4164=ORIENTED_EDGE('',*,*,#3157,.T.);
#4165=ORIENTED_EDGE('',*,*,#3168,.T.);
#4166=ORIENTED_EDGE('',*,*,#3164,.T.);
#4167=ORIENTED_EDGE('',*,*,#3175,.F.);
#4168=ORIENTED_EDGE('',*,*,#3158,.T.);
#4169=ORIENTED_EDGE('',*,*,#3175,.T.);
#4170=ORIENTED_EDGE('',*,*,#3163,.T.);
#4171=ORIENTED_EDGE('',*,*,#3174,.F.);
#4172=ORIENTED_EDGE('',*,*,#3159,.T.);
#4173=ORIENTED_EDGE('',*,*,#3171,.T.);
#4174=ORIENTED_EDGE('',*,*,#3154,.T.);
#4175=ORIENTED_EDGE('',*,*,#3173,.F.);
#4838=CYLINDRICAL_SURFACE('',#5710,0.25175);
#5006=ADVANCED_FACE('',(#805),#256,.T.);
#5007=ADVANCED_FACE('',(#806),#257,.T.);
#5008=ADVANCED_FACE('',(#807),#566,.T.);
#5009=ADVANCED_FACE('',(#808),#567,.T.);
#5010=ADVANCED_FACE('',(#809),#568,.T.);
#5011=ADVANCED_FACE('',(#810),#4838,.F.);
#5012=ADVANCED_FACE('',(#811),#569,.T.);
#5013=ADVANCED_FACE('',(#812),#570,.T.);
#5014=ADVANCED_FACE('',(#813),#571,.T.);
#5015=ADVANCED_FACE('',(#814,#449),#572,.T.);
#5016=ADVANCED_FACE('',(#815,#450),#573,.F.);
#5177=CLOSED_SHELL('',(#5006,#5007,#5008,#5009,#5010,#5011,#5012,#5013,
#5014,#5015,#5016));
#5702=AXIS2_PLACEMENT_3D('',#8261,#6726,#6727);
#5703=AXIS2_PLACEMENT_3D('',#8262,#6728,#6729);
#5704=AXIS2_PLACEMENT_3D('',#8274,#6731,#6732);
#5705=AXIS2_PLACEMENT_3D('',#8290,#6733,#6734);
#5706=AXIS2_PLACEMENT_3D('',#8292,#6735,#6736);
#5707=AXIS2_PLACEMENT_3D('',#8318,#6738,#6739);
#5708=AXIS2_PLACEMENT_3D('',#8321,#6742,#6743);
#5709=AXIS2_PLACEMENT_3D('',#8323,#6745,#6746);
#5710=AXIS2_PLACEMENT_3D('',#8325,#6748,#6749);
#5711=AXIS2_PLACEMENT_3D('',#8327,#6750,#6751);
#5712=AXIS2_PLACEMENT_3D('',#8330,#6753,#6754);
#5713=AXIS2_PLACEMENT_3D('',#8331,#6755,#6756);
#5714=AXIS2_PLACEMENT_3D('',#8333,#6758,#6759);
#5715=AXIS2_PLACEMENT_3D('',#8335,#6761,#6762);
#5716=AXIS2_PLACEMENT_3D('',#8336,#6763,#6764);
#5717=AXIS2_PLACEMENT_3D('',#8337,#6765,#6766);
#6726=DIRECTION('axis',(0.,0.,1.));
#6727=DIRECTION('refdir',(1.,0.,0.));
#6728=DIRECTION('center_axis',(0.,1.,0.));
#6729=DIRECTION('ref_axis',(1.,0.,0.));
#6730=DIRECTION('',(0.866025403784439,-0.5,1.06057523872491E-16));
#6731=DIRECTION('center_axis',(0.,-1.,0.));
#6732=DIRECTION('ref_axis',(1.,0.,0.));
#6733=DIRECTION('center_axis',(0.,-1.,0.));
#6734=DIRECTION('ref_axis',(1.,0.,0.));
#6735=DIRECTION('center_axis',(0.,1.,0.));
#6736=DIRECTION('ref_axis',(1.,0.,0.));
#6737=DIRECTION('',(-0.866025403784439,-0.5,-1.06057523872491E-16));
#6738=DIRECTION('center_axis',(1.92296268638356E-16,0.,-1.));
#6739=DIRECTION('ref_axis',(-1.,0.,-1.92296268638356E-16));
#6740=DIRECTION('',(0.,1.,0.));
#6741=DIRECTION('',(0.,1.,0.));
#6742=DIRECTION('center_axis',(-0.866025403784439,0.,-0.5));
#6743=DIRECTION('ref_axis',(-0.5,0.,0.866025403784439));
#6744=DIRECTION('',(0.,1.,0.));
#6745=DIRECTION('center_axis',(-0.866025403784439,0.,0.5));
#6746=DIRECTION('ref_axis',(0.5,0.,0.866025403784439));
#6747=DIRECTION('',(0.,1.,0.));
#6748=DIRECTION('center_axis',(0.,1.,0.));
#6749=DIRECTION('ref_axis',(1.,0.,0.));
#6750=DIRECTION('center_axis',(0.,1.,0.));
#6751=DIRECTION('ref_axis',(1.,0.,0.));
#6752=DIRECTION('',(0.,-1.,0.));
#6753=DIRECTION('center_axis',(0.,1.,0.));
#6754=DIRECTION('ref_axis',(1.,0.,0.));
#6755=DIRECTION('center_axis',(-1.92296268638356E-16,0.,1.));
#6756=DIRECTION('ref_axis',(1.,0.,1.92296268638356E-16));
#6757=DIRECTION('',(0.,1.,0.));
#6758=DIRECTION('center_axis',(0.866025403784439,0.,-0.5));
#6759=DIRECTION('ref_axis',(-0.5,0.,-0.866025403784439));
#6760=DIRECTION('',(0.,1.,0.));
#6761=DIRECTION('center_axis',(0.866025403784439,0.,0.5));
#6762=DIRECTION('ref_axis',(0.5,0.,-0.866025403784439));
#6763=DIRECTION('center_axis',(0.,1.,0.));
#6764=DIRECTION('ref_axis',(1.,0.,0.));
#6765=DIRECTION('center_axis',(0.,1.,0.));
#6766=DIRECTION('ref_axis',(1.,0.,0.));
#8261=CARTESIAN_POINT('',(0.,0.,0.));
#8262=CARTESIAN_POINT('Origin',(0.,0.0584134911936118,0.));
#8263=CARTESIAN_POINT('',(-0.288675134594813,0.0590919554682611,0.5));
#8264=CARTESIAN_POINT('',(0.288675134594813,0.0590919554682611,0.5));
#8265=CARTESIAN_POINT('Ctrl Pts',(-0.288675134594813,0.0590919554682611,
0.5));
#8266=CARTESIAN_POINT('Ctrl Pts',(2.1664336991023E-12,-0.0242413778636964,
0.5));
#8267=CARTESIAN_POINT('Ctrl Pts',(0.288675134594813,0.0590919554682611,
0.5));
#8268=CARTESIAN_POINT('',(-0.577350269189626,0.0590919554682611,-7.07050159149938E-17));
#8269=CARTESIAN_POINT('Ctrl Pts',(-0.577350269189626,0.0590919554682611,
-7.07050159149938E-17));
#8270=CARTESIAN_POINT('Ctrl Pts',(-0.433012701891136,-0.0242413778636963,
0.250000000001876));
#8271=CARTESIAN_POINT('Ctrl Pts',(-0.288675134594813,0.0590919554682611,
0.5));
#8272=CARTESIAN_POINT('',(-0.475,-4.16333634234434E-17,-5.81707229594993E-17));
#8273=CARTESIAN_POINT('',(-0.576175134594813,0.0584134911936118,-7.05611034329833E-17));
#8274=CARTESIAN_POINT('Origin',(0.,0.,0.));
#8275=CARTESIAN_POINT('',(-0.288675134594813,0.0590919554682611,-0.5));
#8276=CARTESIAN_POINT('Ctrl Pts',(-0.288675134594813,0.0590919554682611,
-0.5));
#8277=CARTESIAN_POINT('Ctrl Pts',(-0.433012701893303,-0.0242413778636963,
-0.249999999998124));
#8278=CARTESIAN_POINT('Ctrl Pts',(-0.577350269189626,0.0590919554682611,
-7.07050159149938E-17));
#8279=CARTESIAN_POINT('',(0.288675134594813,0.0590919554682611,-0.5));
#8280=CARTESIAN_POINT('Ctrl Pts',(0.288675134594813,0.0590919554682611,
-0.5));
#8281=CARTESIAN_POINT('Ctrl Pts',(-2.16648921025353E-12,-0.0242413778636962,
-0.5));
#8282=CARTESIAN_POINT('Ctrl Pts',(-0.288675134594813,0.0590919554682611,
-0.5));
#8283=CARTESIAN_POINT('',(0.577350269189626,0.0590919554682611,0.));
#8284=CARTESIAN_POINT('Ctrl Pts',(0.577350269189626,0.0590919554682611,
0.));
#8285=CARTESIAN_POINT('Ctrl Pts',(0.433012701891136,-0.0242413778636963,
-0.250000000001876));
#8286=CARTESIAN_POINT('Ctrl Pts',(0.288675134594813,0.0590919554682611,
-0.5));
#8287=CARTESIAN_POINT('Ctrl Pts',(0.288675134594813,0.0590919554682611,
0.5));
#8288=CARTESIAN_POINT('Ctrl Pts',(0.433012701893303,-0.0242413778636962,
0.249999999998124));
#8289=CARTESIAN_POINT('Ctrl Pts',(0.577350269189626,0.0590919554682611,
0.));
#8290=CARTESIAN_POINT('Origin',(0.,0.461586508806388,0.));
#8291=CARTESIAN_POINT('',(-0.475,0.52,-5.81707229594993E-17));
#8292=CARTESIAN_POINT('Origin',(0.,0.52,0.));
#8293=CARTESIAN_POINT('',(-0.577350269189626,0.460908044531739,-7.07050159149938E-17));
#8294=CARTESIAN_POINT('',(-0.576175134594813,0.461586508806388,-7.05611034329833E-17));
#8295=CARTESIAN_POINT('',(-0.288675134594813,0.460908044531739,0.5));
#8296=CARTESIAN_POINT('Ctrl Pts',(-0.288675134594813,0.460908044531739,
0.5));
#8297=CARTESIAN_POINT('Ctrl Pts',(-0.433012701893303,0.544241377863696,
0.249999999998124));
#8298=CARTESIAN_POINT('Ctrl Pts',(-0.577350269189626,0.460908044531739,
-7.07050159149938E-17));
#8299=CARTESIAN_POINT('',(0.288675134594813,0.460908044531739,0.5));
#8300=CARTESIAN_POINT('Ctrl Pts',(0.288675134594813,0.460908044531739,0.5));
#8301=CARTESIAN_POINT('Ctrl Pts',(-2.16676676600969E-12,0.544241377863697,
0.5));
#8302=CARTESIAN_POINT('Ctrl Pts',(-0.288675134594813,0.460908044531739,
0.5));
#8303=CARTESIAN_POINT('',(0.577350269189626,0.460908044531739,0.));
#8304=CARTESIAN_POINT('Ctrl Pts',(0.577350269189626,0.460908044531739,0.));
#8305=CARTESIAN_POINT('Ctrl Pts',(0.433012701891136,0.544241377863696,0.250000000001876));
#8306=CARTESIAN_POINT('Ctrl Pts',(0.288675134594813,0.460908044531739,0.5));
#8307=CARTESIAN_POINT('',(0.288675134594813,0.460908044531739,-0.5));
#8308=CARTESIAN_POINT('Ctrl Pts',(0.288675134594813,0.460908044531739,-0.5));
#8309=CARTESIAN_POINT('Ctrl Pts',(0.433012701893302,0.544241377863696,-0.249999999998124));
#8310=CARTESIAN_POINT('Ctrl Pts',(0.577350269189626,0.460908044531739,0.));
#8311=CARTESIAN_POINT('',(-0.288675134594813,0.460908044531739,-0.5));
#8312=CARTESIAN_POINT('Ctrl Pts',(-0.288675134594813,0.460908044531739,
-0.5));
#8313=CARTESIAN_POINT('Ctrl Pts',(2.16660023255599E-12,0.544241377863697,
-0.5));
#8314=CARTESIAN_POINT('Ctrl Pts',(0.288675134594813,0.460908044531739,-0.5));
#8315=CARTESIAN_POINT('Ctrl Pts',(-0.577350269189626,0.460908044531739,
-7.07050159149938E-17));
#8316=CARTESIAN_POINT('Ctrl Pts',(-0.433012701891136,0.544241377863696,
-0.250000000001876));
#8317=CARTESIAN_POINT('Ctrl Pts',(-0.288675134594813,0.460908044531739,
-0.5));
#8318=CARTESIAN_POINT('Origin',(0.288675134594813,0.,-0.5));
#8319=CARTESIAN_POINT('',(-0.288675134594813,0.,-0.5));
#8320=CARTESIAN_POINT('',(0.288675134594813,0.,-0.5));
#8321=CARTESIAN_POINT('Origin',(-0.288675134594813,0.,-0.5));
#8322=CARTESIAN_POINT('',(-0.577350269189626,0.,-7.07050159149938E-17));
#8323=CARTESIAN_POINT('Origin',(-0.577350269189626,0.,-7.07050159149938E-17));
#8324=CARTESIAN_POINT('',(-0.288675134594813,0.,0.5));
#8325=CARTESIAN_POINT('Origin',(0.,0.,0.));
#8326=CARTESIAN_POINT('',(-0.25175,0.52,3.08304831685346E-17));
#8327=CARTESIAN_POINT('Origin',(0.,0.52,0.));
#8328=CARTESIAN_POINT('',(-0.25175,0.,3.08304831685346E-17));
#8329=CARTESIAN_POINT('',(-0.25175,0.,3.08304831685346E-17));
#8330=CARTESIAN_POINT('Origin',(0.,0.,0.));
#8331=CARTESIAN_POINT('Origin',(-0.288675134594813,0.,0.5));
#8332=CARTESIAN_POINT('',(0.288675134594813,0.,0.5));
#8333=CARTESIAN_POINT('Origin',(0.577350269189626,0.,0.));
#8334=CARTESIAN_POINT('',(0.577350269189626,0.,0.));
#8335=CARTESIAN_POINT('Origin',(0.288675134594813,0.,0.5));
#8336=CARTESIAN_POINT('Origin',(0.,0.52,0.));
#8337=CARTESIAN_POINT('Origin',(0.,0.,0.));
#9235=UNCERTAINTY_MEASURE_WITH_UNIT(LENGTH_MEASURE(0.001),#9286,
'DISTANCE_ACCURACY_VALUE',
'Maximum model space distance between geometric entities at asserted c
onnectivities');
#9255=UNCERTAINTY_MEASURE_WITH_UNIT(LENGTH_MEASURE(0.001),#9286,
'DISTANCE_ACCURACY_VALUE',
'Maximum model space distance between geometric entities at asserted c
onnectivities');
#9265=(
GEOMETRIC_REPRESENTATION_CONTEXT(3)
GLOBAL_UNCERTAINTY_ASSIGNED_CONTEXT((#9235))
GLOBAL_UNIT_ASSIGNED_CONTEXT((#9286,#9288,#9289))
REPRESENTATION_CONTEXT('','3D')
);
#9285=(
GEOMETRIC_REPRESENTATION_CONTEXT(3)
GLOBAL_UNCERTAINTY_ASSIGNED_CONTEXT((#9255))
GLOBAL_UNIT_ASSIGNED_CONTEXT((#9286,#9288,#9289))
REPRESENTATION_CONTEXT('','3D')
);
#9286=(
LENGTH_UNIT()
NAMED_UNIT(*)
SI_UNIT(.CENTI.,.METRE.)
);
#9288=(
NAMED_UNIT(*)
PLANE_ANGLE_UNIT()
SI_UNIT($,.RADIAN.)
);
#9289=(
NAMED_UNIT(*)
SI_UNIT($,.STERADIAN.)
SOLID_ANGLE_UNIT()
);
#9299=SHAPE_DEFINITION_REPRESENTATION(#9328,#9403);
#9328=PRODUCT_DEFINITION_SHAPE('',$,#9433);
#9403=SHAPE_REPRESENTATION('',(#5702),#9265);
#9423=PRODUCT_DEFINITION_CONTEXT('part definition',#9512,'design');
#9433=PRODUCT_DEFINITION('Hex Nut - M6','Hex Nut - M6',#9462,#9423);
#9462=PRODUCT_DEFINITION_FORMATION('',$,#9523);
#9512=APPLICATION_CONTEXT(
'Core Data for Automotive Mechanical Design Process');
#9513=PRODUCT_CONTEXT('part definition',#9512,'mechanical');
#9523=PRODUCT('Hex Nut - M6','Hex Nut - M6','Hex Nut - M6',(#9513));
#9613=COLOUR_RGB('Black',0.12,0.14,0.17);
#9614=FILL_AREA_STYLE_COLOUR('',#9613);
#9615=FILL_AREA_STYLE('',(#9614));
#9616=SURFACE_STYLE_FILL_AREA(#9615);
#9617=SURFACE_SIDE_STYLE('',(#9616));
#9618=SURFACE_STYLE_USAGE(.BOTH.,#9617);
#9619=PRESENTATION_STYLE_ASSIGNMENT((#9618));
ENDSEC;
END-ISO-10303-21;
